ISO-10303-21;
HEADER;
/* Generated by software containing ST-Developer
 * from STEP Tools, Inc. (www.steptools.com) 
 */

FILE_DESCRIPTION(
/* description */ (''),
/* implementation_level */ '2;1');

FILE_NAME(
/* name */ 'Pivot thrust washer.step',
/* time_stamp */ '2026-11-10T08:27:36-08:00',
/* author */ (''),
/* organization */ (''),
/* preprocessor_version */ 'ST-DEVELOPER v20.2',
/* originating_system */ 'Autodesk Translation Framework v15.17.0.0',
/* authorisation */ '');

FILE_SCHEMA (('AUTOMOTIVE_DESIGN { 1 0 10303 214 3 1 1 }'));
ENDSEC;

DATA;
#10=MECHANICAL_DESIGN_GEOMETRIC_PRESENTATION_REPRESENTATION('',(#575),#19090);
#555=SHAPE_REPRESENTATION_RELATIONSHIP('SRR','None',#19146,#565);
#565=ADVANCED_BREP_SHAPE_REPRESENTATION('',(#585),#19089);
#575=STYLED_ITEM('',(#19206),#585);
#585=MANIFOLD_SOLID_BREP('Body1',#6829);
#651=FACE_BOUND('',#1653,.T.);
#652=FACE_BOUND('',#1655,.T.);
#811=PLANE('',#7427);
#812=PLANE('',#7428);
#1197=FACE_OUTER_BOUND('',#1650,.T.);
#1198=FACE_OUTER_BOUND('',#1651,.T.);
#1199=FACE_OUTER_BOUND('',#1652,.T.);
#1200=FACE_OUTER_BOUND('',#1654,.T.);
#1650=EDGE_LOOP('',(#6289,#6290,#6291,#6292));
#1651=EDGE_LOOP('',(#6293,#6294,#6295,#6296));
#1652=EDGE_LOOP('',(#6297));
#1653=EDGE_LOOP('',(#6298));
#1654=EDGE_LOOP('',(#6299));
#1655=EDGE_LOOP('',(#6300));
#2103=LINE('',#19047,#2552);
#2104=LINE('',#19053,#2553);
#2552=VECTOR('',#8848,0.41);
#2553=VECTOR('',#8855,0.6);
#2710=CIRCLE('',#7422,0.41);
#2711=CIRCLE('',#7423,0.41);
#2712=CIRCLE('',#7425,0.6);
#2713=CIRCLE('',#7426,0.6);
#3348=VERTEX_POINT('',#19044);
#3349=VERTEX_POINT('',#19046);
#3350=VERTEX_POINT('',#19050);
#3351=VERTEX_POINT('',#19052);
#4329=EDGE_CURVE('',#3348,#3348,#2710,.T.);
#4330=EDGE_CURVE('',#3348,#3349,#2103,.T.);
#4331=EDGE_CURVE('',#3349,#3349,#2711,.T.);
#4332=EDGE_CURVE('',#3350,#3350,#2712,.T.);
#4333=EDGE_CURVE('',#3350,#3351,#2104,.T.);
#4334=EDGE_CURVE('',#3351,#3351,#2713,.T.);
#6289=ORIENTED_EDGE('',*,*,#4329,.F.);
#6290=ORIENTED_EDGE('',*,*,#4330,.T.);
#6291=ORIENTED_EDGE('',*,*,#4331,.T.);
#6292=ORIENTED_EDGE('',*,*,#4330,.F.);
#6293=ORIENTED_EDGE('',*,*,#4332,.F.);
#6294=ORIENTED_EDGE('',*,*,#4333,.T.);
#6295=ORIENTED_EDGE('',*,*,#4334,.T.);
#6296=ORIENTED_EDGE('',*,*,#4333,.F.);
#6297=ORIENTED_EDGE('',*,*,#4332,.T.);
#6298=ORIENTED_EDGE('',*,*,#4329,.T.);
#6299=ORIENTED_EDGE('',*,*,#4334,.F.);
#6300=ORIENTED_EDGE('',*,*,#4331,.F.);
#6430=CYLINDRICAL_SURFACE('',#7421,0.41);
#6431=CYLINDRICAL_SURFACE('',#7424,0.6);
#6816=ADVANCED_FACE('',(#1197),#6430,.F.);
#6817=ADVANCED_FACE('',(#1198),#6431,.T.);
#6818=ADVANCED_FACE('',(#1199,#651),#811,.T.);
#6819=ADVANCED_FACE('',(#1200,#652),#812,.F.);
#6829=CLOSED_SHELL('',(#6816,#6817,#6818,#6819));
#7420=AXIS2_PLACEMENT_3D('',#19042,#8842,#8843);
#7421=AXIS2_PLACEMENT_3D('',#19043,#8844,#8845);
#7422=AXIS2_PLACEMENT_3D('',#19045,#8846,#8847);
#7423=AXIS2_PLACEMENT_3D('',#19048,#8849,#8850);
#7424=AXIS2_PLACEMENT_3D('',#19049,#8851,#8852);
#7425=AXIS2_PLACEMENT_3D('',#19051,#8853,#8854);
#7426=AXIS2_PLACEMENT_3D('',#19054,#8856,#8857);
#7427=AXIS2_PLACEMENT_3D('',#19055,#8858,#8859);
#7428=AXIS2_PLACEMENT_3D('',#19056,#8860,#8861);
#8842=DIRECTION('axis',(0.,0.,1.));
#8843=DIRECTION('refdir',(1.,0.,0.));
#8844=DIRECTION('center_axis',(0.,0.,1.));
#8845=DIRECTION('ref_axis',(1.,0.,0.));
#8846=DIRECTION('center_axis',(0.,0.,-1.));
#8847=DIRECTION('ref_axis',(1.,0.,0.));
#8848=DIRECTION('',(0.,0.,-1.));
#8849=DIRECTION('center_axis',(0.,0.,-1.));
#8850=DIRECTION('ref_axis',(1.,0.,0.));
#8851=DIRECTION('center_axis',(0.,0.,1.));
#8852=DIRECTION('ref_axis',(1.,0.,0.));
#8853=DIRECTION('center_axis',(0.,0.,1.));
#8854=DIRECTION('ref_axis',(1.,0.,0.));
#8855=DIRECTION('',(0.,0.,-1.));
#8856=DIRECTION('center_axis',(0.,0.,1.));
#8857=DIRECTION('ref_axis',(1.,0.,0.));
#8858=DIRECTION('center_axis',(0.,0.,1.));
#8859=DIRECTION('ref_axis',(1.,0.,0.));
#8860=DIRECTION('center_axis',(0.,0.,1.));
#8861=DIRECTION('ref_axis',(1.,0.,0.));
#19042=CARTESIAN_POINT('',(0.,0.,0.));
#19043=CARTESIAN_POINT('Origin',(0.,0.,0.));
#19044=CARTESIAN_POINT('',(-0.41,-5.02105187650415E-17,0.1));
#19045=CARTESIAN_POINT('Origin',(0.,0.,0.1));
#19046=CARTESIAN_POINT('',(-0.41,-5.02105187650415E-17,0.));
#19047=CARTESIAN_POINT('',(-0.41,-5.02105187650415E-17,0.));
#19048=CARTESIAN_POINT('Origin',(0.,0.,0.));
#19049=CARTESIAN_POINT('Origin',(0.,0.,0.));
#19050=CARTESIAN_POINT('',(-0.6,-7.34788079488412E-17,0.1));
#19051=CARTESIAN_POINT('Origin',(0.,0.,0.1));
#19052=CARTESIAN_POINT('',(-0.6,-7.34788079488412E-17,0.));
#19053=CARTESIAN_POINT('',(-0.6,-7.34788079488412E-17,0.));
#19054=CARTESIAN_POINT('Origin',(0.,0.,0.));
#19055=CARTESIAN_POINT('Origin',(0.,0.,0.1));
#19056=CARTESIAN_POINT('Origin',(0.,0.,0.));
#19076=UNCERTAINTY_MEASURE_WITH_UNIT(LENGTH_MEASURE(0.001),#19091,
'DISTANCE_ACCURACY_VALUE',
'Maximum model space distance between geometric entities at asserted c
onnectivities');
#19077=UNCERTAINTY_MEASURE_WITH_UNIT(LENGTH_MEASURE(0.001),#19091,
'DISTANCE_ACCURACY_VALUE',
'Maximum model space distance between geometric entities at asserted c
onnectivities');
#19089=(
GEOMETRIC_REPRESENTATION_CONTEXT(3)
GLOBAL_UNCERTAINTY_ASSIGNED_CONTEXT((#19076))
GLOBAL_UNIT_ASSIGNED_CONTEXT((#19091,#19093,#19094))
REPRESENTATION_CONTEXT('','3D')
);
#19090=(
GEOMETRIC_REPRESENTATION_CONTEXT(3)
GLOBAL_UNCERTAINTY_ASSIGNED_CONTEXT((#19077))
GLOBAL_UNIT_ASSIGNED_CONTEXT((#19091,#19093,#19094))
REPRESENTATION_CONTEXT('','3D')
);
#19091=(
LENGTH_UNIT()
NAMED_UNIT(*)
SI_UNIT(.CENTI.,.METRE.)
);
#19093=(
NAMED_UNIT(*)
PLANE_ANGLE_UNIT()
SI_UNIT($,.RADIAN.)
);
#19094=(
NAMED_UNIT(*)
SI_UNIT($,.STERADIAN.)
SOLID_ANGLE_UNIT()
);
#19106=SHAPE_DEFINITION_REPRESENTATION(#19126,#19146);
#19126=PRODUCT_DEFINITION_SHAPE('',$,#19159);
#19146=SHAPE_REPRESENTATION('',(#7420),#19089);
#19147=PRODUCT_DEFINITION_CONTEXT('part definition',#19185,'design');
#19159=PRODUCT_DEFINITION('Pivot thrust washer','Pivot thrust washer',#19171,
#19147);
#19171=PRODUCT_DEFINITION_FORMATION('',$,#19198);
#19185=APPLICATION_CONTEXT(
'Core Data for Automotive Mechanical Design Process');
#19186=PRODUCT_CONTEXT('part definition',#19185,'mechanical');
#19198=PRODUCT('Pivot thrust washer','Pivot thrust washer',$,(#19186));
#19206=PRESENTATION_STYLE_ASSIGNMENT((#19214));
#19214=SURFACE_STYLE_USAGE(.BOTH.,#19222);
#19222=SURFACE_SIDE_STYLE('',(#19230));
#19230=SURFACE_STYLE_FILL_AREA(#19238);
#19238=FILL_AREA_STYLE('Washer gray',(#19246));
#19246=FILL_AREA_STYLE_COLOUR('Washer gray',#19254);
#19254=COLOUR_RGB('Washer gray',0.725490196078431,0.752941176470588,0.792156862745098);
ENDSEC;
END-ISO-10303-21;
